ISO-10303-21;
HEADER;
/* Generated by software containing ST-Developer
 * from STEP Tools, Inc. (www.steptools.com) 
 */

FILE_DESCRIPTION(
/* description */ (''),
/* implementation_level */ '2;1');

FILE_NAME(
/* name */ 'Nut.step',
/* time_stamp */ '2026-10-06T12:47:13-07:00',
/* author */ (''),
/* organization */ (''),
/* preprocessor_version */ 'ST-DEVELOPER v20.2',
/* originating_system */ 'Autodesk Translation Framework v15.15.0.0',
/* authorisation */ '');

FILE_SCHEMA (('AUTOMOTIVE_DESIGN { 1 0 10303 214 3 1 1 }'));
ENDSEC;

DATA;
#10=MECHANICAL_DESIGN_GEOMETRIC_PRESENTATION_REPRESENTATION('',(#73),#42667);
#55=SHAPE_REPRESENTATION_RELATIONSHIP('SRR','None',#42708,#64);
#64=ADVANCED_BREP_SHAPE_REPRESENTATION('',(#82),#42664);
#73=STYLED_ITEM('',(#42756),#82);
#82=MANIFOLD_SOLID_BREP('Body1',#4038);
#390=FACE_BOUND('',#959,.T.);
#391=FACE_BOUND('',#967,.T.);
#455=CYLINDRICAL_SURFACE('',#4306,4.);
#571=CIRCLE('',#4307,4.);
#572=CIRCLE('',#4308,4.);
#748=FACE_OUTER_BOUND('',#957,.T.);
#749=FACE_OUTER_BOUND('',#958,.T.);
#750=FACE_OUTER_BOUND('',#960,.T.);
#751=FACE_OUTER_BOUND('',#961,.T.);
#752=FACE_OUTER_BOUND('',#962,.T.);
#753=FACE_OUTER_BOUND('',#963,.T.);
#754=FACE_OUTER_BOUND('',#964,.T.);
#755=FACE_OUTER_BOUND('',#965,.T.);
#756=FACE_OUTER_BOUND('',#966,.T.);
#957=EDGE_LOOP('',(#3290,#3291,#3292,#3293));
#958=EDGE_LOOP('',(#3294,#3295,#3296,#3297,#3298,#3299));
#959=EDGE_LOOP('',(#3300));
#960=EDGE_LOOP('',(#3301,#3302,#3303,#3304));
#961=EDGE_LOOP('',(#3305,#3306,#3307,#3308));
#962=EDGE_LOOP('',(#3309,#3310,#3311,#3312));
#963=EDGE_LOOP('',(#3313,#3314,#3315,#3316));
#964=EDGE_LOOP('',(#3317,#3318,#3319,#3320));
#965=EDGE_LOOP('',(#3321,#3322,#3323,#3324));
#966=EDGE_LOOP('',(#3325,#3326,#3327,#3328,#3329,#3330));
#967=EDGE_LOOP('',(#3331));
#1166=LINE('',#33580,#1379);
#1167=LINE('',#33585,#1380);
#1168=LINE('',#33587,#1381);
#1169=LINE('',#33589,#1382);
#1170=LINE('',#33591,#1383);
#1171=LINE('',#33593,#1384);
#1172=LINE('',#33594,#1385);
#1173=LINE('',#33597,#1386);
#1174=LINE('',#33599,#1387);
#1175=LINE('',#33600,#1388);
#1176=LINE('',#33603,#1389);
#1177=LINE('',#33604,#1390);
#1178=LINE('',#33607,#1391);
#1179=LINE('',#33608,#1392);
#1180=LINE('',#33611,#1393);
#1181=LINE('',#33612,#1394);
#1182=LINE('',#33615,#1395);
#1183=LINE('',#33616,#1396);
#1184=LINE('',#33618,#1397);
#1379=VECTOR('',#4917,4.);
#1380=VECTOR('',#4922,10.);
#1381=VECTOR('',#4923,10.);
#1382=VECTOR('',#4924,10.);
#1383=VECTOR('',#4925,10.);
#1384=VECTOR('',#4926,9.99999999999999);
#1385=VECTOR('',#4927,10.);
#1386=VECTOR('',#4930,10.);
#1387=VECTOR('',#4931,10.);
#1388=VECTOR('',#4932,10.);
#1389=VECTOR('',#4935,10.);
#1390=VECTOR('',#4936,10.);
#1391=VECTOR('',#4939,10.);
#1392=VECTOR('',#4940,10.);
#1393=VECTOR('',#4943,9.99999999999999);
#1394=VECTOR('',#4944,10.);
#1395=VECTOR('',#4947,10.);
#1396=VECTOR('',#4948,10.);
#1397=VECTOR('',#4951,10.);
#1761=VERTEX_POINT('',#33577);
#1762=VERTEX_POINT('',#33579);
#1763=VERTEX_POINT('',#33583);
#1764=VERTEX_POINT('',#33584);
#1765=VERTEX_POINT('',#33586);
#1766=VERTEX_POINT('',#33588);
#1767=VERTEX_POINT('',#33590);
#1768=VERTEX_POINT('',#33592);
#1769=VERTEX_POINT('',#33596);
#1770=VERTEX_POINT('',#33598);
#1771=VERTEX_POINT('',#33602);
#1772=VERTEX_POINT('',#33606);
#1773=VERTEX_POINT('',#33610);
#1774=VERTEX_POINT('',#33614);
#2296=EDGE_CURVE('',#1761,#1761,#571,.T.);
#2297=EDGE_CURVE('',#1761,#1762,#1166,.T.);
#2298=EDGE_CURVE('',#1762,#1762,#572,.T.);
#2299=EDGE_CURVE('',#1763,#1764,#1167,.T.);
#2300=EDGE_CURVE('',#1764,#1765,#1168,.T.);
#2301=EDGE_CURVE('',#1765,#1766,#1169,.T.);
#2302=EDGE_CURVE('',#1766,#1767,#1170,.T.);
#2303=EDGE_CURVE('',#1767,#1768,#1171,.T.);
#2304=EDGE_CURVE('',#1768,#1763,#1172,.T.);
#2305=EDGE_CURVE('',#1769,#1764,#1173,.T.);
#2306=EDGE_CURVE('',#1770,#1769,#1174,.T.);
#2307=EDGE_CURVE('',#1770,#1765,#1175,.T.);
#2308=EDGE_CURVE('',#1771,#1770,#1176,.T.);
#2309=EDGE_CURVE('',#1771,#1766,#1177,.T.);
#2310=EDGE_CURVE('',#1772,#1771,#1178,.T.);
#2311=EDGE_CURVE('',#1772,#1767,#1179,.T.);
#2312=EDGE_CURVE('',#1773,#1772,#1180,.T.);
#2313=EDGE_CURVE('',#1773,#1768,#1181,.T.);
#2314=EDGE_CURVE('',#1774,#1773,#1182,.T.);
#2315=EDGE_CURVE('',#1763,#1774,#1183,.T.);
#2316=EDGE_CURVE('',#1769,#1774,#1184,.T.);
#3290=ORIENTED_EDGE('',*,*,#2296,.F.);
#3291=ORIENTED_EDGE('',*,*,#2297,.T.);
#3292=ORIENTED_EDGE('',*,*,#2298,.F.);
#3293=ORIENTED_EDGE('',*,*,#2297,.F.);
#3294=ORIENTED_EDGE('',*,*,#2299,.T.);
#3295=ORIENTED_EDGE('',*,*,#2300,.T.);
#3296=ORIENTED_EDGE('',*,*,#2301,.T.);
#3297=ORIENTED_EDGE('',*,*,#2302,.T.);
#3298=ORIENTED_EDGE('',*,*,#2303,.T.);
#3299=ORIENTED_EDGE('',*,*,#2304,.T.);
#3300=ORIENTED_EDGE('',*,*,#2298,.T.);
#3301=ORIENTED_EDGE('',*,*,#2305,.F.);
#3302=ORIENTED_EDGE('',*,*,#2306,.F.);
#3303=ORIENTED_EDGE('',*,*,#2307,.T.);
#3304=ORIENTED_EDGE('',*,*,#2300,.F.);
#3305=ORIENTED_EDGE('',*,*,#2307,.F.);
#3306=ORIENTED_EDGE('',*,*,#2308,.F.);
#3307=ORIENTED_EDGE('',*,*,#2309,.T.);
#3308=ORIENTED_EDGE('',*,*,#2301,.F.);
#3309=ORIENTED_EDGE('',*,*,#2309,.F.);
#3310=ORIENTED_EDGE('',*,*,#2310,.F.);
#3311=ORIENTED_EDGE('',*,*,#2311,.T.);
#3312=ORIENTED_EDGE('',*,*,#2302,.F.);
#3313=ORIENTED_EDGE('',*,*,#2311,.F.);
#3314=ORIENTED_EDGE('',*,*,#2312,.F.);
#3315=ORIENTED_EDGE('',*,*,#2313,.T.);
#3316=ORIENTED_EDGE('',*,*,#2303,.F.);
#3317=ORIENTED_EDGE('',*,*,#2313,.F.);
#3318=ORIENTED_EDGE('',*,*,#2314,.F.);
#3319=ORIENTED_EDGE('',*,*,#2315,.F.);
#3320=ORIENTED_EDGE('',*,*,#2304,.F.);
#3321=ORIENTED_EDGE('',*,*,#2315,.T.);
#3322=ORIENTED_EDGE('',*,*,#2316,.F.);
#3323=ORIENTED_EDGE('',*,*,#2305,.T.);
#3324=ORIENTED_EDGE('',*,*,#2299,.F.);
#3325=ORIENTED_EDGE('',*,*,#2316,.T.);
#3326=ORIENTED_EDGE('',*,*,#2314,.T.);
#3327=ORIENTED_EDGE('',*,*,#2312,.T.);
#3328=ORIENTED_EDGE('',*,*,#2310,.T.);
#3329=ORIENTED_EDGE('',*,*,#2308,.T.);
#3330=ORIENTED_EDGE('',*,*,#2306,.T.);
#3331=ORIENTED_EDGE('',*,*,#2296,.T.);
#3809=PLANE('',#4309);
#3810=PLANE('',#4310);
#3811=PLANE('',#4311);
#3812=PLANE('',#4312);
#3813=PLANE('',#4313);
#3814=PLANE('',#4314);
#3815=PLANE('',#4315);
#3816=PLANE('',#4316);
#3944=ADVANCED_FACE('',(#748),#455,.F.);
#3945=ADVANCED_FACE('',(#749,#390),#3809,.T.);
#3946=ADVANCED_FACE('',(#750),#3810,.T.);
#3947=ADVANCED_FACE('',(#751),#3811,.T.);
#3948=ADVANCED_FACE('',(#752),#3812,.T.);
#3949=ADVANCED_FACE('',(#753),#3813,.T.);
#3950=ADVANCED_FACE('',(#754),#3814,.T.);
#3951=ADVANCED_FACE('',(#755),#3815,.T.);
#3952=ADVANCED_FACE('',(#756,#391),#3816,.T.);
#4038=CLOSED_SHELL('',(#3944,#3945,#3946,#3947,#3948,#3949,#3950,#3951,
#3952));
#4305=AXIS2_PLACEMENT_3D('',#33575,#4911,#4912);
#4306=AXIS2_PLACEMENT_3D('',#33576,#4913,#4914);
#4307=AXIS2_PLACEMENT_3D('',#33578,#4915,#4916);
#4308=AXIS2_PLACEMENT_3D('',#33581,#4918,#4919);
#4309=AXIS2_PLACEMENT_3D('',#33582,#4920,#4921);
#4310=AXIS2_PLACEMENT_3D('',#33595,#4928,#4929);
#4311=AXIS2_PLACEMENT_3D('',#33601,#4933,#4934);
#4312=AXIS2_PLACEMENT_3D('',#33605,#4937,#4938);
#4313=AXIS2_PLACEMENT_3D('',#33609,#4941,#4942);
#4314=AXIS2_PLACEMENT_3D('',#33613,#4945,#4946);
#4315=AXIS2_PLACEMENT_3D('',#33617,#4949,#4950);
#4316=AXIS2_PLACEMENT_3D('',#33619,#4952,#4953);
#4911=DIRECTION('axis',(0.,0.,1.));
#4912=DIRECTION('refdir',(1.,0.,0.));
#4913=DIRECTION('center_axis',(0.,0.,1.));
#4914=DIRECTION('ref_axis',(-1.,0.,0.));
#4915=DIRECTION('center_axis',(0.,0.,1.));
#4916=DIRECTION('ref_axis',(-1.,0.,0.));
#4917=DIRECTION('',(0.,0.,1.));
#4918=DIRECTION('center_axis',(0.,0.,-1.));
#4919=DIRECTION('ref_axis',(-1.,0.,0.));
#4920=DIRECTION('center_axis',(0.,0.,1.));
#4921=DIRECTION('ref_axis',(1.,0.,0.));
#4922=DIRECTION('',(1.,-6.40987562127854E-16,0.));
#4923=DIRECTION('',(0.5,0.866025403784439,0.));
#4924=DIRECTION('',(-0.5,0.866025403784439,0.));
#4925=DIRECTION('',(-1.,3.20493781063927E-16,0.));
#4926=DIRECTION('',(-0.5,-0.866025403784439,0.));
#4927=DIRECTION('',(0.499999999999999,-0.866025403784439,0.));
#4928=DIRECTION('center_axis',(0.866025403784439,-0.5,0.));
#4929=DIRECTION('ref_axis',(-0.5,-0.866025403784439,0.));
#4930=DIRECTION('',(0.,0.,1.));
#4931=DIRECTION('',(-0.5,-0.866025403784439,0.));
#4932=DIRECTION('',(0.,0.,1.));
#4933=DIRECTION('center_axis',(0.866025403784439,0.5,0.));
#4934=DIRECTION('ref_axis',(0.5,-0.866025403784439,0.));
#4935=DIRECTION('',(0.5,-0.866025403784439,0.));
#4936=DIRECTION('',(0.,0.,1.));
#4937=DIRECTION('center_axis',(3.20493781063927E-16,1.,0.));
#4938=DIRECTION('ref_axis',(1.,-3.20493781063927E-16,0.));
#4939=DIRECTION('',(1.,-3.20493781063927E-16,0.));
#4940=DIRECTION('',(0.,0.,1.));
#4941=DIRECTION('center_axis',(-0.866025403784438,0.5,0.));
#4942=DIRECTION('ref_axis',(0.5,0.866025403784438,0.));
#4943=DIRECTION('',(0.5,0.866025403784439,0.));
#4944=DIRECTION('',(0.,0.,1.));
#4945=DIRECTION('center_axis',(-0.866025403784439,-0.5,0.));
#4946=DIRECTION('ref_axis',(-0.5,0.866025403784439,0.));
#4947=DIRECTION('',(-0.499999999999999,0.866025403784439,0.));
#4948=DIRECTION('',(0.,0.,-1.));
#4949=DIRECTION('center_axis',(-6.40987562127854E-16,-1.,0.));
#4950=DIRECTION('ref_axis',(-1.,6.40987562127854E-16,0.));
#4951=DIRECTION('',(-1.,6.40987562127854E-16,0.));
#4952=DIRECTION('center_axis',(0.,0.,-1.));
#4953=DIRECTION('ref_axis',(-1.,0.,0.));
#33575=CARTESIAN_POINT('',(0.,0.,0.));
#33576=CARTESIAN_POINT('Origin',(0.,0.,32.));
#33577=CARTESIAN_POINT('',(4.,4.89858719658941E-16,29.));
#33578=CARTESIAN_POINT('Origin',(0.,0.,29.));
#33579=CARTESIAN_POINT('',(4.,-4.89858719658941E-16,35.));
#33580=CARTESIAN_POINT('',(4.,4.89858719658941E-16,32.));
#33581=CARTESIAN_POINT('Origin',(0.,0.,35.));
#33582=CARTESIAN_POINT('Origin',(0.,0.,35.));
#33583=CARTESIAN_POINT('',(-3.46410161513776,-6.,35.));
#33584=CARTESIAN_POINT('',(3.46410161513775,-6.,35.));
#33585=CARTESIAN_POINT('',(-3.46410161513776,-6.,35.));
#33586=CARTESIAN_POINT('',(6.92820323027551,-2.22044604925031E-15,35.));
#33587=CARTESIAN_POINT('',(3.46410161513775,-6.,35.));
#33588=CARTESIAN_POINT('',(3.46410161513776,6.,35.));
#33589=CARTESIAN_POINT('',(6.92820323027551,-2.22044604925031E-15,35.));
#33590=CARTESIAN_POINT('',(-3.46410161513775,6.,35.));
#33591=CARTESIAN_POINT('',(3.46410161513776,6.,35.));
#33592=CARTESIAN_POINT('',(-6.92820323027551,4.44089209850063E-15,35.));
#33593=CARTESIAN_POINT('',(-3.46410161513775,6.,35.));
#33594=CARTESIAN_POINT('',(-6.92820323027551,3.88578058618805E-15,35.));
#33595=CARTESIAN_POINT('Origin',(6.92820323027551,-2.22044604925031E-15,
32.));
#33596=CARTESIAN_POINT('',(3.46410161513775,-6.,29.));
#33597=CARTESIAN_POINT('',(3.46410161513775,-6.,32.));
#33598=CARTESIAN_POINT('',(6.92820323027551,-2.22044604925031E-15,29.));
#33599=CARTESIAN_POINT('',(3.46410161513775,-6.,29.));
#33600=CARTESIAN_POINT('',(6.92820323027551,-2.22044604925031E-15,32.));
#33601=CARTESIAN_POINT('Origin',(3.46410161513776,6.,32.));
#33602=CARTESIAN_POINT('',(3.46410161513776,6.,29.));
#33603=CARTESIAN_POINT('',(6.92820323027551,-2.22044604925031E-15,29.));
#33604=CARTESIAN_POINT('',(3.46410161513776,6.,32.));
#33605=CARTESIAN_POINT('Origin',(-3.46410161513775,6.,32.));
#33606=CARTESIAN_POINT('',(-3.46410161513775,6.,29.));
#33607=CARTESIAN_POINT('',(3.46410161513776,6.,29.));
#33608=CARTESIAN_POINT('',(-3.46410161513775,6.,32.));
#33609=CARTESIAN_POINT('Origin',(-6.92820323027551,4.44089209850063E-15,
32.));
#33610=CARTESIAN_POINT('',(-6.92820323027551,4.44089209850063E-15,29.));
#33611=CARTESIAN_POINT('',(-3.46410161513775,6.,29.));
#33612=CARTESIAN_POINT('',(-6.92820323027551,3.88578058618805E-15,32.));
#33613=CARTESIAN_POINT('Origin',(-3.46410161513776,-6.,32.));
#33614=CARTESIAN_POINT('',(-3.46410161513776,-6.,29.));
#33615=CARTESIAN_POINT('',(-6.92820323027551,3.88578058618805E-15,29.));
#33616=CARTESIAN_POINT('',(-3.46410161513776,-6.,32.));
#33617=CARTESIAN_POINT('Origin',(3.46410161513775,-6.,32.));
#33618=CARTESIAN_POINT('',(-3.46410161513776,-6.,29.));
#33619=CARTESIAN_POINT('Origin',(0.,0.,29.));
#42653=UNCERTAINTY_MEASURE_WITH_UNIT(LENGTH_MEASURE(0.01),#42668,
'DISTANCE_ACCURACY_VALUE',
'Maximum model space distance between geometric entities at asserted c
onnectivities');
#42656=UNCERTAINTY_MEASURE_WITH_UNIT(LENGTH_MEASURE(0.01),#42668,
'DISTANCE_ACCURACY_VALUE',
'Maximum model space distance between geometric entities at asserted c
onnectivities');
#42664=(
GEOMETRIC_REPRESENTATION_CONTEXT(3)
GLOBAL_UNCERTAINTY_ASSIGNED_CONTEXT((#42653))
GLOBAL_UNIT_ASSIGNED_CONTEXT((#42668,#42670,#42671))
REPRESENTATION_CONTEXT('','3D')
);
#42667=(
GEOMETRIC_REPRESENTATION_CONTEXT(3)
GLOBAL_UNCERTAINTY_ASSIGNED_CONTEXT((#42656))
GLOBAL_UNIT_ASSIGNED_CONTEXT((#42668,#42670,#42671))
REPRESENTATION_CONTEXT('','3D')
);
#42668=(
LENGTH_UNIT()
NAMED_UNIT(*)
SI_UNIT(.MILLI.,.METRE.)
);
#42670=(
NAMED_UNIT(*)
PLANE_ANGLE_UNIT()
SI_UNIT($,.RADIAN.)
);
#42671=(
NAMED_UNIT(*)
SI_UNIT($,.STERADIAN.)
SOLID_ANGLE_UNIT()
);
#42679=SHAPE_DEFINITION_REPRESENTATION(#42689,#42708);
#42689=PRODUCT_DEFINITION_SHAPE('',$,#42719);
#42708=SHAPE_REPRESENTATION('',(#4305),#42664);
#42711=PRODUCT_DEFINITION_CONTEXT('part definition',#42743,'design');
#42719=PRODUCT_DEFINITION('Nut','Nut',#42729,#42711);
#42729=PRODUCT_DEFINITION_FORMATION('',$,#42752);
#42743=APPLICATION_CONTEXT(
'Core Data for Automotive Mechanical Design Process');
#42744=PRODUCT_CONTEXT('part definition',#42743,'mechanical');
#42752=PRODUCT('Nut','Nut',$,(#42744));
#42756=PRESENTATION_STYLE_ASSIGNMENT((#42758));
#42758=SURFACE_STYLE_USAGE(.BOTH.,#42760);
#42760=SURFACE_SIDE_STYLE('',(#42762));
#42762=SURFACE_STYLE_FILL_AREA(#42764);
#42764=FILL_AREA_STYLE('Opaque(160,160,160)',(#42766));
#42766=FILL_AREA_STYLE_COLOUR('Opaque(160,160,160)',#42768);
#42768=COLOUR_RGB('Opaque(160,160,160)', 0.09019608, 0.27058824, 0.51372549);
ENDSEC;
END-ISO-10303-21;
